ISO-10303-21;
HEADER;
/* Generated by software containing ST-Developer
 * from STEP Tools, Inc. (www.steptools.com) 
 */

FILE_DESCRIPTION(
/* description */ ('Belt-driven linear axis on 2020 extrusion'),
/* implementation_level */ '2;1');

FILE_NAME(
/* name */ 'Captive slot nut.step',
/* time_stamp */ '2026-10-28T03:26:09-07:00',
/* author */ (''),
/* organization */ (''),
/* preprocessor_version */ 'ST-DEVELOPER v20.2',
/* originating_system */ 'Autodesk Translation Framework v15.17.0.0',
/* authorisation */ '');

FILE_SCHEMA (('AUTOMOTIVE_DESIGN { 1 0 10303 214 3 1 1 }'));
ENDSEC;

DATA;
#10=MECHANICAL_DESIGN_GEOMETRIC_PRESENTATION_REPRESENTATION('',(#640),#20096);
#19=ELLIPSE('',#12111,0.299389011154384,0.2117);
#20=ELLIPSE('',#12115,0.299389011154384,0.2117);
#538=SHAPE_REPRESENTATION_RELATIONSHIP('SRR','None',#20335,#584);
#584=ADVANCED_BREP_SHAPE_REPRESENTATION('',(#696),#20066);
#640=STYLED_ITEM('',(#20657),#696);
#696=MANIFOLD_SOLID_BREP('Body1',#10953);
#815=FACE_BOUND('',#2284,.T.);
#1068=PLANE('',#12101);
#1069=PLANE('',#12102);
#1070=PLANE('',#12103);
#1071=PLANE('',#12105);
#1072=PLANE('',#12106);
#1073=PLANE('',#12107);
#1074=PLANE('',#12108);
#1075=PLANE('',#12109);
#1076=PLANE('',#12110);
#1077=PLANE('',#12117);
#1078=PLANE('',#12118);
#1079=PLANE('',#12119);
#1080=PLANE('',#12120);
#1562=FACE_OUTER_BOUND('',#2281,.T.);
#1563=FACE_OUTER_BOUND('',#2282,.T.);
#1564=FACE_OUTER_BOUND('',#2283,.T.);
#1565=FACE_OUTER_BOUND('',#2285,.T.);
#1566=FACE_OUTER_BOUND('',#2286,.T.);
#1567=FACE_OUTER_BOUND('',#2287,.T.);
#1568=FACE_OUTER_BOUND('',#2288,.T.);
#1569=FACE_OUTER_BOUND('',#2289,.T.);
#1570=FACE_OUTER_BOUND('',#2290,.T.);
#1571=FACE_OUTER_BOUND('',#2291,.T.);
#1572=FACE_OUTER_BOUND('',#2292,.T.);
#1573=FACE_OUTER_BOUND('',#2293,.T.);
#1574=FACE_OUTER_BOUND('',#2294,.T.);
#1575=FACE_OUTER_BOUND('',#2295,.T.);
#2281=EDGE_LOOP('',(#8707,#8708,#8709,#8710));
#2282=EDGE_LOOP('',(#8711,#8712,#8713,#8714));
#2283=EDGE_LOOP('',(#8715,#8716,#8717,#8718));
#2284=EDGE_LOOP('',(#8719));
#2285=EDGE_LOOP('',(#8720,#8721,#8722,#8723,#8724,#8725,#8726,#8727,#8728,
#8729));
#2286=EDGE_LOOP('',(#8730,#8731,#8732,#8733));
#2287=EDGE_LOOP('',(#8734,#8735,#8736,#8737));
#2288=EDGE_LOOP('',(#8738,#8739,#8740,#8741,#8742,#8743,#8744,#8745,#8746,
#8747));
#2289=EDGE_LOOP('',(#8748,#8749,#8750,#8751));
#2290=EDGE_LOOP('',(#8752,#8753,#8754,#8755,#8756,#8757));
#2291=EDGE_LOOP('',(#8758,#8759,#8760,#8761,#8762,#8763,#8764,#8765));
#2292=EDGE_LOOP('',(#8766,#8767,#8768,#8769,#8770));
#2293=EDGE_LOOP('',(#8771,#8772,#8773,#8774));
#2294=EDGE_LOOP('',(#8775,#8776,#8777,#8778,#8779,#8780));
#2295=EDGE_LOOP('',(#8781,#8782,#8783,#8784));
#3104=LINE('',#18135,#3961);
#3105=LINE('',#18137,#3962);
#3106=LINE('',#18139,#3963);
#3107=LINE('',#18140,#3964);
#3108=LINE('',#18143,#3965);
#3109=LINE('',#18145,#3966);
#3110=LINE('',#18146,#3967);
#3111=LINE('',#18149,#3968);
#3112=LINE('',#18151,#3969);
#3113=LINE('',#18152,#3970);
#3114=LINE('',#18157,#3971);
#3115=LINE('',#18159,#3972);
#3116=LINE('',#18161,#3973);
#3117=LINE('',#18163,#3974);
#3118=LINE('',#18165,#3975);
#3119=LINE('',#18167,#3976);
#3120=LINE('',#18168,#3977);
#3121=LINE('',#18171,#3978);
#3122=LINE('',#18172,#3979);
#3123=LINE('',#18175,#3980);
#3124=LINE('',#18176,#3981);
#3125=LINE('',#18179,#3982);
#3126=LINE('',#18181,#3983);
#3127=LINE('',#18183,#3984);
#3128=LINE('',#18185,#3985);
#3129=LINE('',#18186,#3986);
#3130=LINE('',#18188,#3987);
#3131=LINE('',#18191,#3988);
#3132=LINE('',#18194,#3989);
#3133=LINE('',#18198,#3990);
#3134=LINE('',#18205,#3991);
#3135=LINE('',#18207,#3992);
#3136=LINE('',#18209,#3993);
#3961=VECTOR('',#14448,1.);
#3962=VECTOR('',#14449,1.);
#3963=VECTOR('',#14450,1.);
#3964=VECTOR('',#14451,1.);
#3965=VECTOR('',#14454,1.);
#3966=VECTOR('',#14455,1.);
#3967=VECTOR('',#14456,1.);
#3968=VECTOR('',#14459,1.);
#3969=VECTOR('',#14460,1.);
#3970=VECTOR('',#14461,1.);
#3971=VECTOR('',#14466,1.);
#3972=VECTOR('',#14467,1.);
#3973=VECTOR('',#14468,1.);
#3974=VECTOR('',#14469,1.);
#3975=VECTOR('',#14470,1.);
#3976=VECTOR('',#14471,1.);
#3977=VECTOR('',#14472,1.);
#3978=VECTOR('',#14475,1.);
#3979=VECTOR('',#14476,1.);
#3980=VECTOR('',#14479,1.);
#3981=VECTOR('',#14480,1.);
#3982=VECTOR('',#14483,1.);
#3983=VECTOR('',#14484,1.);
#3984=VECTOR('',#14485,1.);
#3985=VECTOR('',#14486,1.);
#3986=VECTOR('',#14487,1.);
#3987=VECTOR('',#14490,1.);
#3988=VECTOR('',#14493,1.);
#3989=VECTOR('',#14496,1.);
#3990=VECTOR('',#14501,0.21);
#3991=VECTOR('',#14510,1.);
#3992=VECTOR('',#14513,1.);
#3993=VECTOR('',#14516,1.);
#4649=CIRCLE('',#12104,0.2117);
#4650=CIRCLE('',#12113,0.2117);
#4651=CIRCLE('',#12114,0.2117);
#4652=CIRCLE('',#12116,0.2117);
#5386=VERTEX_POINT('',#18133);
#5387=VERTEX_POINT('',#18134);
#5388=VERTEX_POINT('',#18136);
#5389=VERTEX_POINT('',#18138);
#5390=VERTEX_POINT('',#18142);
#5391=VERTEX_POINT('',#18144);
#5392=VERTEX_POINT('',#18148);
#5393=VERTEX_POINT('',#18150);
#5394=VERTEX_POINT('',#18153);
#5395=VERTEX_POINT('',#18156);
#5396=VERTEX_POINT('',#18158);
#5397=VERTEX_POINT('',#18160);
#5398=VERTEX_POINT('',#18162);
#5399=VERTEX_POINT('',#18164);
#5400=VERTEX_POINT('',#18166);
#5401=VERTEX_POINT('',#18170);
#5402=VERTEX_POINT('',#18174);
#5403=VERTEX_POINT('',#18178);
#5404=VERTEX_POINT('',#18180);
#5405=VERTEX_POINT('',#18182);
#5406=VERTEX_POINT('',#18184);
#5407=VERTEX_POINT('',#18190);
#5408=VERTEX_POINT('',#18192);
#5409=VERTEX_POINT('',#18196);
#5410=VERTEX_POINT('',#18199);
#5411=VERTEX_POINT('',#18201);
#6568=EDGE_CURVE('',#5386,#5387,#3104,.T.);
#6569=EDGE_CURVE('',#5388,#5386,#3105,.T.);
#6570=EDGE_CURVE('',#5389,#5388,#3106,.T.);
#6571=EDGE_CURVE('',#5387,#5389,#3107,.T.);
#6572=EDGE_CURVE('',#5388,#5390,#3108,.T.);
#6573=EDGE_CURVE('',#5391,#5390,#3109,.T.);
#6574=EDGE_CURVE('',#5389,#5391,#3110,.T.);
#6575=EDGE_CURVE('',#5390,#5392,#3111,.T.);
#6576=EDGE_CURVE('',#5392,#5393,#3112,.T.);
#6577=EDGE_CURVE('',#5393,#5391,#3113,.T.);
#6578=EDGE_CURVE('',#5394,#5394,#4649,.T.);
#6579=EDGE_CURVE('',#5395,#5386,#3114,.T.);
#6580=EDGE_CURVE('',#5396,#5395,#3115,.T.);
#6581=EDGE_CURVE('',#5396,#5397,#3116,.T.);
#6582=EDGE_CURVE('',#5398,#5397,#3117,.T.);
#6583=EDGE_CURVE('',#5398,#5399,#3118,.T.);
#6584=EDGE_CURVE('',#5399,#5400,#3119,.T.);
#6585=EDGE_CURVE('',#5400,#5392,#3120,.T.);
#6586=EDGE_CURVE('',#5400,#5401,#3121,.T.);
#6587=EDGE_CURVE('',#5401,#5393,#3122,.T.);
#6588=EDGE_CURVE('',#5402,#5399,#3123,.T.);
#6589=EDGE_CURVE('',#5401,#5402,#3124,.T.);
#6590=EDGE_CURVE('',#5403,#5402,#3125,.T.);
#6591=EDGE_CURVE('',#5404,#5403,#3126,.T.);
#6592=EDGE_CURVE('',#5404,#5405,#3127,.T.);
#6593=EDGE_CURVE('',#5406,#5405,#3128,.T.);
#6594=EDGE_CURVE('',#5406,#5387,#3129,.T.);
#6595=EDGE_CURVE('',#5403,#5398,#3130,.T.);
#6596=EDGE_CURVE('',#5397,#5407,#3131,.T.);
#6597=EDGE_CURVE('',#5407,#5408,#19,.T.);
#6598=EDGE_CURVE('',#5408,#5404,#3132,.T.);
#6599=EDGE_CURVE('',#5409,#5407,#4650,.F.);
#6600=EDGE_CURVE('',#5409,#5394,#3133,.T.);
#6601=EDGE_CURVE('',#5410,#5409,#4651,.F.);
#6602=EDGE_CURVE('',#5411,#5410,#20,.T.);
#6603=EDGE_CURVE('',#5408,#5411,#4652,.F.);
#6604=EDGE_CURVE('',#5410,#5396,#3134,.T.);
#6605=EDGE_CURVE('',#5405,#5411,#3135,.T.);
#6606=EDGE_CURVE('',#5395,#5406,#3136,.T.);
#8707=ORIENTED_EDGE('',*,*,#6568,.F.);
#8708=ORIENTED_EDGE('',*,*,#6569,.F.);
#8709=ORIENTED_EDGE('',*,*,#6570,.F.);
#8710=ORIENTED_EDGE('',*,*,#6571,.F.);
#8711=ORIENTED_EDGE('',*,*,#6570,.T.);
#8712=ORIENTED_EDGE('',*,*,#6572,.T.);
#8713=ORIENTED_EDGE('',*,*,#6573,.F.);
#8714=ORIENTED_EDGE('',*,*,#6574,.F.);
#8715=ORIENTED_EDGE('',*,*,#6575,.T.);
#8716=ORIENTED_EDGE('',*,*,#6576,.T.);
#8717=ORIENTED_EDGE('',*,*,#6577,.T.);
#8718=ORIENTED_EDGE('',*,*,#6573,.T.);
#8719=ORIENTED_EDGE('',*,*,#6578,.T.);
#8720=ORIENTED_EDGE('',*,*,#6575,.F.);
#8721=ORIENTED_EDGE('',*,*,#6572,.F.);
#8722=ORIENTED_EDGE('',*,*,#6569,.T.);
#8723=ORIENTED_EDGE('',*,*,#6579,.F.);
#8724=ORIENTED_EDGE('',*,*,#6580,.F.);
#8725=ORIENTED_EDGE('',*,*,#6581,.T.);
#8726=ORIENTED_EDGE('',*,*,#6582,.F.);
#8727=ORIENTED_EDGE('',*,*,#6583,.T.);
#8728=ORIENTED_EDGE('',*,*,#6584,.T.);
#8729=ORIENTED_EDGE('',*,*,#6585,.T.);
#8730=ORIENTED_EDGE('',*,*,#6586,.T.);
#8731=ORIENTED_EDGE('',*,*,#6587,.T.);
#8732=ORIENTED_EDGE('',*,*,#6576,.F.);
#8733=ORIENTED_EDGE('',*,*,#6585,.F.);
#8734=ORIENTED_EDGE('',*,*,#6588,.F.);
#8735=ORIENTED_EDGE('',*,*,#6589,.F.);
#8736=ORIENTED_EDGE('',*,*,#6586,.F.);
#8737=ORIENTED_EDGE('',*,*,#6584,.F.);
#8738=ORIENTED_EDGE('',*,*,#6577,.F.);
#8739=ORIENTED_EDGE('',*,*,#6587,.F.);
#8740=ORIENTED_EDGE('',*,*,#6589,.T.);
#8741=ORIENTED_EDGE('',*,*,#6590,.F.);
#8742=ORIENTED_EDGE('',*,*,#6591,.F.);
#8743=ORIENTED_EDGE('',*,*,#6592,.T.);
#8744=ORIENTED_EDGE('',*,*,#6593,.F.);
#8745=ORIENTED_EDGE('',*,*,#6594,.T.);
#8746=ORIENTED_EDGE('',*,*,#6571,.T.);
#8747=ORIENTED_EDGE('',*,*,#6574,.T.);
#8748=ORIENTED_EDGE('',*,*,#6588,.T.);
#8749=ORIENTED_EDGE('',*,*,#6583,.F.);
#8750=ORIENTED_EDGE('',*,*,#6595,.F.);
#8751=ORIENTED_EDGE('',*,*,#6590,.T.);
#8752=ORIENTED_EDGE('',*,*,#6591,.T.);
#8753=ORIENTED_EDGE('',*,*,#6595,.T.);
#8754=ORIENTED_EDGE('',*,*,#6582,.T.);
#8755=ORIENTED_EDGE('',*,*,#6596,.T.);
#8756=ORIENTED_EDGE('',*,*,#6597,.T.);
#8757=ORIENTED_EDGE('',*,*,#6598,.T.);
#8758=ORIENTED_EDGE('',*,*,#6597,.F.);
#8759=ORIENTED_EDGE('',*,*,#6599,.F.);
#8760=ORIENTED_EDGE('',*,*,#6600,.T.);
#8761=ORIENTED_EDGE('',*,*,#6578,.F.);
#8762=ORIENTED_EDGE('',*,*,#6600,.F.);
#8763=ORIENTED_EDGE('',*,*,#6601,.F.);
#8764=ORIENTED_EDGE('',*,*,#6602,.F.);
#8765=ORIENTED_EDGE('',*,*,#6603,.F.);
#8766=ORIENTED_EDGE('',*,*,#6596,.F.);
#8767=ORIENTED_EDGE('',*,*,#6581,.F.);
#8768=ORIENTED_EDGE('',*,*,#6604,.F.);
#8769=ORIENTED_EDGE('',*,*,#6601,.T.);
#8770=ORIENTED_EDGE('',*,*,#6599,.T.);
#8771=ORIENTED_EDGE('',*,*,#6598,.F.);
#8772=ORIENTED_EDGE('',*,*,#6603,.T.);
#8773=ORIENTED_EDGE('',*,*,#6605,.F.);
#8774=ORIENTED_EDGE('',*,*,#6592,.F.);
#8775=ORIENTED_EDGE('',*,*,#6580,.T.);
#8776=ORIENTED_EDGE('',*,*,#6606,.T.);
#8777=ORIENTED_EDGE('',*,*,#6593,.T.);
#8778=ORIENTED_EDGE('',*,*,#6605,.T.);
#8779=ORIENTED_EDGE('',*,*,#6602,.T.);
#8780=ORIENTED_EDGE('',*,*,#6604,.T.);
#8781=ORIENTED_EDGE('',*,*,#6568,.T.);
#8782=ORIENTED_EDGE('',*,*,#6594,.F.);
#8783=ORIENTED_EDGE('',*,*,#6606,.F.);
#8784=ORIENTED_EDGE('',*,*,#6579,.T.);
#10188=CYLINDRICAL_SURFACE('',#12112,0.2117);
#10613=ADVANCED_FACE('',(#1562),#1068,.F.);
#10614=ADVANCED_FACE('',(#1563),#1069,.T.);
#10615=ADVANCED_FACE('',(#1564,#815),#1070,.T.);
#10616=ADVANCED_FACE('',(#1565),#1071,.T.);
#10617=ADVANCED_FACE('',(#1566),#1072,.T.);
#10618=ADVANCED_FACE('',(#1567),#1073,.F.);
#10619=ADVANCED_FACE('',(#1568),#1074,.T.);
#10620=ADVANCED_FACE('',(#1569),#1075,.T.);
#10621=ADVANCED_FACE('',(#1570),#1076,.T.);
#10622=ADVANCED_FACE('',(#1571),#10188,.F.);
#10623=ADVANCED_FACE('',(#1572),#1077,.F.);
#10624=ADVANCED_FACE('',(#1573),#1078,.F.);
#10625=ADVANCED_FACE('',(#1574),#1079,.T.);
#10626=ADVANCED_FACE('',(#1575),#1080,.T.);
#10953=CLOSED_SHELL('',(#10613,#10614,#10615,#10616,#10617,#10618,#10619,
#10620,#10621,#10622,#10623,#10624,#10625,#10626));
#12100=AXIS2_PLACEMENT_3D('',#18131,#14444,#14445);
#12101=AXIS2_PLACEMENT_3D('',#18132,#14446,#14447);
#12102=AXIS2_PLACEMENT_3D('',#18141,#14452,#14453);
#12103=AXIS2_PLACEMENT_3D('',#18147,#14457,#14458);
#12104=AXIS2_PLACEMENT_3D('',#18154,#14462,#14463);
#12105=AXIS2_PLACEMENT_3D('',#18155,#14464,#14465);
#12106=AXIS2_PLACEMENT_3D('',#18169,#14473,#14474);
#12107=AXIS2_PLACEMENT_3D('',#18173,#14477,#14478);
#12108=AXIS2_PLACEMENT_3D('',#18177,#14481,#14482);
#12109=AXIS2_PLACEMENT_3D('',#18187,#14488,#14489);
#12110=AXIS2_PLACEMENT_3D('',#18189,#14491,#14492);
#12111=AXIS2_PLACEMENT_3D('',#18193,#14494,#14495);
#12112=AXIS2_PLACEMENT_3D('',#18195,#14497,#14498);
#12113=AXIS2_PLACEMENT_3D('',#18197,#14499,#14500);
#12114=AXIS2_PLACEMENT_3D('',#18200,#14502,#14503);
#12115=AXIS2_PLACEMENT_3D('',#18202,#14504,#14505);
#12116=AXIS2_PLACEMENT_3D('',#18203,#14506,#14507);
#12117=AXIS2_PLACEMENT_3D('',#18204,#14508,#14509);
#12118=AXIS2_PLACEMENT_3D('',#18206,#14511,#14512);
#12119=AXIS2_PLACEMENT_3D('',#18208,#14514,#14515);
#12120=AXIS2_PLACEMENT_3D('',#18210,#14517,#14518);
#14444=DIRECTION('axis',(0.,0.,1.));
#14445=DIRECTION('refdir',(1.,0.,0.));
#14446=DIRECTION('center_axis',(0.,0.,1.));
#14447=DIRECTION('ref_axis',(1.,0.,0.));
#14448=DIRECTION('',(1.,0.,0.));
#14449=DIRECTION('',(0.,-1.,0.));
#14450=DIRECTION('',(-1.,0.,0.));
#14451=DIRECTION('',(0.,1.,0.));
#14452=DIRECTION('center_axis',(0.,1.,0.));
#14453=DIRECTION('ref_axis',(-1.,0.,0.));
#14454=DIRECTION('',(0.,0.,1.));
#14455=DIRECTION('',(-1.,0.,0.));
#14456=DIRECTION('',(0.,0.,1.));
#14457=DIRECTION('center_axis',(0.,0.,1.));
#14458=DIRECTION('ref_axis',(1.,0.,0.));
#14459=DIRECTION('',(0.,-1.,0.));
#14460=DIRECTION('',(1.,0.,0.));
#14461=DIRECTION('',(0.,1.,0.));
#14462=DIRECTION('center_axis',(0.,0.,-1.));
#14463=DIRECTION('ref_axis',(1.,0.,0.));
#14464=DIRECTION('center_axis',(-1.,0.,0.));
#14465=DIRECTION('ref_axis',(0.,-1.,0.));
#14466=DIRECTION('',(0.,0.,1.));
#14467=DIRECTION('',(0.,0.707106781186548,0.707106781186548));
#14468=DIRECTION('',(0.,-1.,0.));
#14469=DIRECTION('',(0.,0.707106781186548,-0.707106781186548));
#14470=DIRECTION('',(0.,0.,1.));
#14471=DIRECTION('',(0.,-1.,0.));
#14472=DIRECTION('',(0.,0.,1.));
#14473=DIRECTION('center_axis',(0.,-1.,0.));
#14474=DIRECTION('ref_axis',(1.,0.,0.));
#14475=DIRECTION('',(1.,0.,0.));
#14476=DIRECTION('',(0.,0.,1.));
#14477=DIRECTION('center_axis',(0.,0.,1.));
#14478=DIRECTION('ref_axis',(1.,0.,0.));
#14479=DIRECTION('',(-1.,0.,0.));
#14480=DIRECTION('',(0.,1.,0.));
#14481=DIRECTION('center_axis',(1.,0.,0.));
#14482=DIRECTION('ref_axis',(0.,1.,0.));
#14483=DIRECTION('',(0.,0.,1.));
#14484=DIRECTION('',(0.,-0.707106781186548,0.707106781186548));
#14485=DIRECTION('',(0.,1.,0.));
#14486=DIRECTION('',(0.,-0.707106781186548,-0.707106781186548));
#14487=DIRECTION('',(0.,0.,1.));
#14488=DIRECTION('center_axis',(0.,-1.,0.));
#14489=DIRECTION('ref_axis',(1.,0.,0.));
#14490=DIRECTION('',(-1.,0.,0.));
#14491=DIRECTION('center_axis',(0.,-0.707106781186548,-0.707106781186548));
#14492=DIRECTION('ref_axis',(-1.,0.,0.));
#14493=DIRECTION('',(1.,0.,0.));
#14494=DIRECTION('center_axis',(0.,0.707106781186548,0.707106781186548));
#14495=DIRECTION('ref_axis',(0.,0.707106781186547,-0.707106781186547));
#14496=DIRECTION('',(1.,0.,0.));
#14497=DIRECTION('center_axis',(0.,0.,1.));
#14498=DIRECTION('ref_axis',(1.,0.,0.));
#14499=DIRECTION('center_axis',(0.,0.,-1.));
#14500=DIRECTION('ref_axis',(1.,0.,0.));
#14501=DIRECTION('',(0.,0.,1.));
#14502=DIRECTION('center_axis',(0.,0.,-1.));
#14503=DIRECTION('ref_axis',(1.,0.,0.));
#14504=DIRECTION('center_axis',(0.,-0.707106781186548,0.707106781186548));
#14505=DIRECTION('ref_axis',(0.,0.707106781186547,0.707106781186547));
#14506=DIRECTION('center_axis',(0.,0.,-1.));
#14507=DIRECTION('ref_axis',(1.,0.,0.));
#14508=DIRECTION('center_axis',(0.,0.,1.));
#14509=DIRECTION('ref_axis',(1.,0.,0.));
#14510=DIRECTION('',(-1.,0.,0.));
#14511=DIRECTION('center_axis',(0.,0.,1.));
#14512=DIRECTION('ref_axis',(1.,0.,0.));
#14513=DIRECTION('',(-1.,0.,0.));
#14514=DIRECTION('center_axis',(0.,0.707106781186548,-0.707106781186548));
#14515=DIRECTION('ref_axis',(-1.,0.,0.));
#14516=DIRECTION('',(1.,0.,0.));
#14517=DIRECTION('center_axis',(0.,1.,0.));
#14518=DIRECTION('ref_axis',(-1.,0.,0.));
#18131=CARTESIAN_POINT('',(0.,0.,0.));
#18132=CARTESIAN_POINT('Origin',(0.,0.395,0.25));
#18133=CARTESIAN_POINT('',(-0.5,0.3,0.25));
#18134=CARTESIAN_POINT('',(0.5,0.3,0.25));
#18135=CARTESIAN_POINT('',(0.25,0.3,0.25));
#18136=CARTESIAN_POINT('',(-0.5,0.5,0.25));
#18137=CARTESIAN_POINT('',(-0.5,0.5,0.25));
#18138=CARTESIAN_POINT('',(0.5,0.5,0.25));
#18139=CARTESIAN_POINT('',(0.5,0.5,0.25));
#18140=CARTESIAN_POINT('',(0.5,0.29,0.25));
#18141=CARTESIAN_POINT('Origin',(0.5,0.5,0.25));
#18142=CARTESIAN_POINT('',(-0.5,0.5,0.4));
#18143=CARTESIAN_POINT('',(-0.5,0.5,0.25));
#18144=CARTESIAN_POINT('',(0.5,0.5,0.4));
#18145=CARTESIAN_POINT('',(0.5,0.5,0.4));
#18146=CARTESIAN_POINT('',(0.5,0.5,0.25));
#18147=CARTESIAN_POINT('Origin',(0.,0.,0.4));
#18148=CARTESIAN_POINT('',(-0.5,-0.5,0.4));
#18149=CARTESIAN_POINT('',(-0.5,0.5,0.4));
#18150=CARTESIAN_POINT('',(0.5,-0.5,0.4));
#18151=CARTESIAN_POINT('',(-0.5,-0.5,0.4));
#18152=CARTESIAN_POINT('',(0.5,-0.3,0.4));
#18153=CARTESIAN_POINT('',(-0.2117,2.59257727379495E-17,0.4));
#18154=CARTESIAN_POINT('Origin',(0.,0.,0.4));
#18155=CARTESIAN_POINT('Origin',(-0.5,0.3,0.));
#18156=CARTESIAN_POINT('',(-0.5,0.3,0.15));
#18157=CARTESIAN_POINT('',(-0.5,0.3,0.));
#18158=CARTESIAN_POINT('',(-0.5,0.15,0.));
#18159=CARTESIAN_POINT('',(-0.5,0.225,0.075));
#18160=CARTESIAN_POINT('',(-0.5,-0.15,0.));
#18161=CARTESIAN_POINT('',(-0.5,0.3,0.));
#18162=CARTESIAN_POINT('',(-0.5,-0.3,0.15));
#18163=CARTESIAN_POINT('',(-0.5,-0.075,-0.075));
#18164=CARTESIAN_POINT('',(-0.5,-0.3,0.25));
#18165=CARTESIAN_POINT('',(-0.5,-0.3,0.));
#18166=CARTESIAN_POINT('',(-0.5,-0.5,0.25));
#18167=CARTESIAN_POINT('',(-0.5,-0.29,0.25));
#18168=CARTESIAN_POINT('',(-0.5,-0.5,0.25));
#18169=CARTESIAN_POINT('Origin',(-0.5,-0.5,0.25));
#18170=CARTESIAN_POINT('',(0.5,-0.5,0.25));
#18171=CARTESIAN_POINT('',(-0.5,-0.5,0.25));
#18172=CARTESIAN_POINT('',(0.5,-0.5,0.25));
#18173=CARTESIAN_POINT('Origin',(0.,-0.395,0.25));
#18174=CARTESIAN_POINT('',(0.5,-0.3,0.25));
#18175=CARTESIAN_POINT('',(-0.25,-0.3,0.25));
#18176=CARTESIAN_POINT('',(0.5,-0.5,0.25));
#18177=CARTESIAN_POINT('Origin',(0.5,-0.3,0.));
#18178=CARTESIAN_POINT('',(0.5,-0.3,0.15));
#18179=CARTESIAN_POINT('',(0.5,-0.3,0.));
#18180=CARTESIAN_POINT('',(0.5,-0.15,0.));
#18181=CARTESIAN_POINT('',(0.5,-0.225,0.075));
#18182=CARTESIAN_POINT('',(0.5,0.15,0.));
#18183=CARTESIAN_POINT('',(0.5,-0.3,0.));
#18184=CARTESIAN_POINT('',(0.5,0.3,0.15));
#18185=CARTESIAN_POINT('',(0.5,0.075,-0.075));
#18186=CARTESIAN_POINT('',(0.5,0.3,0.));
#18187=CARTESIAN_POINT('Origin',(-0.5,-0.3,0.));
#18188=CARTESIAN_POINT('',(-0.25,-0.3,0.15));
#18189=CARTESIAN_POINT('Origin',(-0.25,-0.225,0.075));
#18190=CARTESIAN_POINT('',(-0.149388386429468,-0.15,0.));
#18191=CARTESIAN_POINT('',(-0.25,-0.15,0.));
#18192=CARTESIAN_POINT('',(0.149388386429468,-0.15,0.));
#18193=CARTESIAN_POINT('Origin',(0.,0.,-0.15));
#18194=CARTESIAN_POINT('',(-0.25,-0.15,0.));
#18195=CARTESIAN_POINT('Origin',(0.,0.,-0.1));
#18196=CARTESIAN_POINT('',(-0.2117,-2.59257727379495E-17,0.));
#18197=CARTESIAN_POINT('Origin',(0.,0.,0.));
#18198=CARTESIAN_POINT('',(-0.2117,-2.59257727379495E-17,-0.1));
#18199=CARTESIAN_POINT('',(-0.149388386429468,0.15,0.));
#18200=CARTESIAN_POINT('Origin',(0.,0.,0.));
#18201=CARTESIAN_POINT('',(0.149388386429468,0.15,0.));
#18202=CARTESIAN_POINT('Origin',(0.,0.,-0.15));
#18203=CARTESIAN_POINT('Origin',(0.,0.,0.));
#18204=CARTESIAN_POINT('Origin',(0.,0.,0.));
#18205=CARTESIAN_POINT('',(0.25,0.15,0.));
#18206=CARTESIAN_POINT('Origin',(0.,0.,0.));
#18207=CARTESIAN_POINT('',(0.25,0.15,0.));
#18208=CARTESIAN_POINT('Origin',(0.25,0.225,0.075));
#18209=CARTESIAN_POINT('',(0.25,0.3,0.15));
#18210=CARTESIAN_POINT('Origin',(0.5,0.3,0.));
#20012=UNCERTAINTY_MEASURE_WITH_UNIT(LENGTH_MEASURE(0.001),#20097,
'DISTANCE_ACCURACY_VALUE',
'Maximum model space distance between geometric entities at asserted c
onnectivities');
#20042=UNCERTAINTY_MEASURE_WITH_UNIT(LENGTH_MEASURE(0.001),#20097,
'DISTANCE_ACCURACY_VALUE',
'Maximum model space distance between geometric entities at asserted c
onnectivities');
#20066=(
GEOMETRIC_REPRESENTATION_CONTEXT(3)
GLOBAL_UNCERTAINTY_ASSIGNED_CONTEXT((#20012))
GLOBAL_UNIT_ASSIGNED_CONTEXT((#20097,#20099,#20100))
REPRESENTATION_CONTEXT('','3D')
);
#20096=(
GEOMETRIC_REPRESENTATION_CONTEXT(3)
GLOBAL_UNCERTAINTY_ASSIGNED_CONTEXT((#20042))
GLOBAL_UNIT_ASSIGNED_CONTEXT((#20097,#20099,#20100))
REPRESENTATION_CONTEXT('','3D')
);
#20097=(
LENGTH_UNIT()
NAMED_UNIT(*)
SI_UNIT(.CENTI.,.METRE.)
);
#20099=(
NAMED_UNIT(*)
PLANE_ANGLE_UNIT()
SI_UNIT($,.RADIAN.)
);
#20100=(
NAMED_UNIT(*)
SI_UNIT($,.STERADIAN.)
SOLID_ANGLE_UNIT()
);
#20124=SHAPE_DEFINITION_REPRESENTATION(#20182,#20335);
#20182=PRODUCT_DEFINITION_SHAPE('',$,#20389);
#20335=SHAPE_REPRESENTATION('',(#12100),#20066);
#20365=PRODUCT_DEFINITION_CONTEXT('part definition',#20526,'design');
#20389=PRODUCT_DEFINITION('Captive slot nut','Captive slot nut',#20442,
#20365);
#20442=PRODUCT_DEFINITION_FORMATION('',$,#20551);
#20526=APPLICATION_CONTEXT(
'Core Data for Automotive Mechanical Design Process');
#20527=PRODUCT_CONTEXT('part definition',#20526,'mechanical');
#20551=PRODUCT('Captive slot nut','Captive slot nut','Captive slot nut',
(#20527));
#20651=COLOUR_RGB('Black',0.12,0.14,0.17);
#20652=FILL_AREA_STYLE_COLOUR('',#20651);
#20653=FILL_AREA_STYLE('',(#20652));
#20654=SURFACE_STYLE_FILL_AREA(#20653);
#20655=SURFACE_SIDE_STYLE('',(#20654));
#20656=SURFACE_STYLE_USAGE(.BOTH.,#20655);
#20657=PRESENTATION_STYLE_ASSIGNMENT((#20656));
ENDSEC;
END-ISO-10303-21;
